ISO-10303-21;
HEADER;
/* Generated by software containing ST-Developer
 * from STEP Tools, Inc. (www.steptools.com) 
 */

FILE_DESCRIPTION(
/* description */ ('Self-centering screw clamp'),
/* implementation_level */ '2;1');

FILE_NAME(
/* name */ 'Screw bearing post (1).step',
/* time_stamp */ '2026-10-28T03:25:31-07:00',
/* author */ (''),
/* organization */ (''),
/* preprocessor_version */ 'ST-DEVELOPER v20.2',
/* originating_system */ 'Autodesk Translation Framework v15.17.0.0',
/* authorisation */ '');

FILE_SCHEMA (('AUTOMOTIVE_DESIGN { 1 0 10303 214 3 1 1 }'));
ENDSEC;

DATA;
#10=MECHANICAL_DESIGN_GEOMETRIC_PRESENTATION_REPRESENTATION('',(#634),#16799);
#552=SHAPE_REPRESENTATION_RELATIONSHIP('SRR','None',#17025,#593);
#593=ADVANCED_BREP_SHAPE_REPRESENTATION('',(#682),#16763);
#634=STYLED_ITEM('',(#17333),#682);
#682=MANIFOLD_SOLID_BREP('Body1',#9085);
#806=FACE_BOUND('',#2012,.T.);
#807=FACE_BOUND('',#2014,.T.);
#808=FACE_BOUND('',#2019,.T.);
#809=FACE_BOUND('',#2020,.T.);
#810=FACE_BOUND('',#2021,.T.);
#811=FACE_BOUND('',#2022,.T.);
#812=FACE_BOUND('',#2023,.T.);
#813=FACE_BOUND('',#2026,.T.);
#814=FACE_BOUND('',#2027,.T.);
#815=FACE_BOUND('',#2028,.T.);
#816=FACE_BOUND('',#2029,.T.);
#817=FACE_BOUND('',#2030,.T.);
#818=FACE_BOUND('',#2033,.T.);
#819=FACE_BOUND('',#2034,.T.);
#1088=PLANE('',#9884);
#1089=PLANE('',#9885);
#1090=PLANE('',#9886);
#1091=PLANE('',#9887);
#1092=PLANE('',#9888);
#1093=PLANE('',#9889);
#1094=PLANE('',#9890);
#1095=PLANE('',#9891);
#1096=PLANE('',#9892);
#1097=PLANE('',#9893);
#1412=FACE_OUTER_BOUND('',#2004,.T.);
#1413=FACE_OUTER_BOUND('',#2005,.T.);
#1414=FACE_OUTER_BOUND('',#2006,.T.);
#1415=FACE_OUTER_BOUND('',#2007,.T.);
#1416=FACE_OUTER_BOUND('',#2008,.T.);
#1417=FACE_OUTER_BOUND('',#2009,.T.);
#1418=FACE_OUTER_BOUND('',#2010,.T.);
#1419=FACE_OUTER_BOUND('',#2011,.T.);
#1420=FACE_OUTER_BOUND('',#2013,.T.);
#1421=FACE_OUTER_BOUND('',#2015,.T.);
#1422=FACE_OUTER_BOUND('',#2016,.T.);
#1423=FACE_OUTER_BOUND('',#2017,.T.);
#1424=FACE_OUTER_BOUND('',#2018,.T.);
#1425=FACE_OUTER_BOUND('',#2024,.T.);
#1426=FACE_OUTER_BOUND('',#2025,.T.);
#1427=FACE_OUTER_BOUND('',#2031,.T.);
#1428=FACE_OUTER_BOUND('',#2032,.T.);
#2004=EDGE_LOOP('',(#6805,#6806,#6807,#6808));
#2005=EDGE_LOOP('',(#6809,#6810,#6811,#6812));
#2006=EDGE_LOOP('',(#6813,#6814,#6815,#6816));
#2007=EDGE_LOOP('',(#6817,#6818,#6819,#6820));
#2008=EDGE_LOOP('',(#6821,#6822,#6823,#6824));
#2009=EDGE_LOOP('',(#6825,#6826,#6827,#6828));
#2010=EDGE_LOOP('',(#6829,#6830,#6831,#6832));
#2011=EDGE_LOOP('',(#6833,#6834,#6835,#6836));
#2012=EDGE_LOOP('',(#6837));
#2013=EDGE_LOOP('',(#6838,#6839,#6840,#6841));
#2014=EDGE_LOOP('',(#6842));
#2015=EDGE_LOOP('',(#6843,#6844,#6845,#6846));
#2016=EDGE_LOOP('',(#6847,#6848,#6849,#6850));
#2017=EDGE_LOOP('',(#6851,#6852,#6853,#6854));
#2018=EDGE_LOOP('',(#6855,#6856,#6857,#6858,#6859,#6860,#6861,#6862));
#2019=EDGE_LOOP('',(#6863));
#2020=EDGE_LOOP('',(#6864));
#2021=EDGE_LOOP('',(#6865));
#2022=EDGE_LOOP('',(#6866));
#2023=EDGE_LOOP('',(#6867));
#2024=EDGE_LOOP('',(#6868,#6869,#6870,#6871));
#2025=EDGE_LOOP('',(#6872,#6873,#6874,#6875,#6876,#6877,#6878,#6879));
#2026=EDGE_LOOP('',(#6880));
#2027=EDGE_LOOP('',(#6881));
#2028=EDGE_LOOP('',(#6882));
#2029=EDGE_LOOP('',(#6883));
#2030=EDGE_LOOP('',(#6884));
#2031=EDGE_LOOP('',(#6885,#6886,#6887,#6888));
#2032=EDGE_LOOP('',(#6889,#6890,#6891,#6892));
#2033=EDGE_LOOP('',(#6893));
#2034=EDGE_LOOP('',(#6894));
#2778=LINE('',#14484,#3351);
#2779=LINE('',#14490,#3352);
#2780=LINE('',#14496,#3353);
#2781=LINE('',#14502,#3354);
#2782=LINE('',#14508,#3355);
#2783=LINE('',#14514,#3356);
#2784=LINE('',#14520,#3357);
#2785=LINE('',#14525,#3358);
#2786=LINE('',#14527,#3359);
#2787=LINE('',#14529,#3360);
#2788=LINE('',#14530,#3361);
#2789=LINE('',#14534,#3362);
#2790=LINE('',#14536,#3363);
#2791=LINE('',#14538,#3364);
#2792=LINE('',#14539,#3365);
#2793=LINE('',#14542,#3366);
#2794=LINE('',#14544,#3367);
#2795=LINE('',#14545,#3368);
#2796=LINE('',#14548,#3369);
#2797=LINE('',#14550,#3370);
#2798=LINE('',#14551,#3371);
#2799=LINE('',#14554,#3372);
#2800=LINE('',#14556,#3373);
#2801=LINE('',#14557,#3374);
#2802=LINE('',#14560,#3375);
#2803=LINE('',#14561,#3376);
#2804=LINE('',#14562,#3377);
#2805=LINE('',#14565,#3378);
#2806=LINE('',#14566,#3379);
#2807=LINE('',#14568,#3380);
#2808=LINE('',#14569,#3381);
#3351=VECTOR('',#11529,0.165);
#3352=VECTOR('',#11536,0.165);
#3353=VECTOR('',#11543,0.165);
#3354=VECTOR('',#11550,0.165);
#3355=VECTOR('',#11557,0.225);
#3356=VECTOR('',#11564,0.225);
#3357=VECTOR('',#11571,1.6);
#3358=VECTOR('',#11576,1.);
#3359=VECTOR('',#11577,1.);
#3360=VECTOR('',#11578,1.);
#3361=VECTOR('',#11579,1.);
#3362=VECTOR('',#11582,1.);
#3363=VECTOR('',#11583,1.);
#3364=VECTOR('',#11584,1.);
#3365=VECTOR('',#11585,1.);
#3366=VECTOR('',#11588,1.);
#3367=VECTOR('',#11589,1.);
#3368=VECTOR('',#11590,1.);
#3369=VECTOR('',#11593,1.);
#3370=VECTOR('',#11594,1.);
#3371=VECTOR('',#11595,1.);
#3372=VECTOR('',#11598,1.);
#3373=VECTOR('',#11599,1.);
#3374=VECTOR('',#11600,1.);
#3375=VECTOR('',#11603,1.);
#3376=VECTOR('',#11604,1.);
#3377=VECTOR('',#11605,1.);
#3378=VECTOR('',#11608,1.);
#3379=VECTOR('',#11609,1.);
#3380=VECTOR('',#11612,1.);
#3381=VECTOR('',#11613,1.);
#3857=CIRCLE('',#9864,0.165);
#3858=CIRCLE('',#9865,0.165);
#3859=CIRCLE('',#9867,0.165);
#3860=CIRCLE('',#9868,0.165);
#3861=CIRCLE('',#9870,0.165);
#3862=CIRCLE('',#9871,0.165);
#3863=CIRCLE('',#9873,0.165);
#3864=CIRCLE('',#9874,0.165);
#3865=CIRCLE('',#9876,0.225);
#3866=CIRCLE('',#9877,0.225);
#3867=CIRCLE('',#9879,0.225);
#3868=CIRCLE('',#9880,0.225);
#3869=CIRCLE('',#9882,1.6);
#3870=CIRCLE('',#9883,1.6);
#4455=VERTEX_POINT('',#14481);
#4456=VERTEX_POINT('',#14483);
#4457=VERTEX_POINT('',#14487);
#4458=VERTEX_POINT('',#14489);
#4459=VERTEX_POINT('',#14493);
#4460=VERTEX_POINT('',#14495);
#4461=VERTEX_POINT('',#14499);
#4462=VERTEX_POINT('',#14501);
#4463=VERTEX_POINT('',#14505);
#4464=VERTEX_POINT('',#14507);
#4465=VERTEX_POINT('',#14511);
#4466=VERTEX_POINT('',#14513);
#4467=VERTEX_POINT('',#14517);
#4468=VERTEX_POINT('',#14519);
#4469=VERTEX_POINT('',#14523);
#4470=VERTEX_POINT('',#14524);
#4471=VERTEX_POINT('',#14526);
#4472=VERTEX_POINT('',#14528);
#4473=VERTEX_POINT('',#14532);
#4474=VERTEX_POINT('',#14533);
#4475=VERTEX_POINT('',#14535);
#4476=VERTEX_POINT('',#14537);
#4477=VERTEX_POINT('',#14541);
#4478=VERTEX_POINT('',#14543);
#4479=VERTEX_POINT('',#14547);
#4480=VERTEX_POINT('',#14549);
#4481=VERTEX_POINT('',#14553);
#4482=VERTEX_POINT('',#14555);
#4483=VERTEX_POINT('',#14559);
#4484=VERTEX_POINT('',#14564);
#5327=EDGE_CURVE('',#4455,#4455,#3857,.T.);
#5328=EDGE_CURVE('',#4455,#4456,#2778,.T.);
#5329=EDGE_CURVE('',#4456,#4456,#3858,.T.);
#5330=EDGE_CURVE('',#4457,#4457,#3859,.T.);
#5331=EDGE_CURVE('',#4457,#4458,#2779,.T.);
#5332=EDGE_CURVE('',#4458,#4458,#3860,.T.);
#5333=EDGE_CURVE('',#4459,#4459,#3861,.T.);
#5334=EDGE_CURVE('',#4459,#4460,#2780,.T.);
#5335=EDGE_CURVE('',#4460,#4460,#3862,.T.);
#5336=EDGE_CURVE('',#4461,#4461,#3863,.T.);
#5337=EDGE_CURVE('',#4461,#4462,#2781,.T.);
#5338=EDGE_CURVE('',#4462,#4462,#3864,.T.);
#5339=EDGE_CURVE('',#4463,#4463,#3865,.T.);
#5340=EDGE_CURVE('',#4463,#4464,#2782,.T.);
#5341=EDGE_CURVE('',#4464,#4464,#3866,.T.);
#5342=EDGE_CURVE('',#4465,#4465,#3867,.T.);
#5343=EDGE_CURVE('',#4465,#4466,#2783,.T.);
#5344=EDGE_CURVE('',#4466,#4466,#3868,.T.);
#5345=EDGE_CURVE('',#4467,#4467,#3869,.T.);
#5346=EDGE_CURVE('',#4467,#4468,#2784,.T.);
#5347=EDGE_CURVE('',#4468,#4468,#3870,.T.);
#5348=EDGE_CURVE('',#4469,#4470,#2785,.T.);
#5349=EDGE_CURVE('',#4471,#4469,#2786,.T.);
#5350=EDGE_CURVE('',#4472,#4471,#2787,.T.);
#5351=EDGE_CURVE('',#4472,#4470,#2788,.T.);
#5352=EDGE_CURVE('',#4473,#4474,#2789,.T.);
#5353=EDGE_CURVE('',#4473,#4475,#2790,.T.);
#5354=EDGE_CURVE('',#4475,#4476,#2791,.T.);
#5355=EDGE_CURVE('',#4474,#4476,#2792,.T.);
#5356=EDGE_CURVE('',#4477,#4472,#2793,.T.);
#5357=EDGE_CURVE('',#4478,#4471,#2794,.T.);
#5358=EDGE_CURVE('',#4477,#4478,#2795,.T.);
#5359=EDGE_CURVE('',#4475,#4479,#2796,.T.);
#5360=EDGE_CURVE('',#4479,#4480,#2797,.T.);
#5361=EDGE_CURVE('',#4476,#4480,#2798,.T.);
#5362=EDGE_CURVE('',#4474,#4481,#2799,.T.);
#5363=EDGE_CURVE('',#4482,#4481,#2800,.T.);
#5364=EDGE_CURVE('',#4473,#4482,#2801,.T.);
#5365=EDGE_CURVE('',#4469,#4483,#2802,.T.);
#5366=EDGE_CURVE('',#4481,#4483,#2803,.T.);
#5367=EDGE_CURVE('',#4480,#4478,#2804,.T.);
#5368=EDGE_CURVE('',#4470,#4484,#2805,.T.);
#5369=EDGE_CURVE('',#4483,#4484,#2806,.T.);
#5370=EDGE_CURVE('',#4484,#4482,#2807,.T.);
#5371=EDGE_CURVE('',#4477,#4479,#2808,.T.);
#6805=ORIENTED_EDGE('',*,*,#5327,.F.);
#6806=ORIENTED_EDGE('',*,*,#5328,.T.);
#6807=ORIENTED_EDGE('',*,*,#5329,.F.);
#6808=ORIENTED_EDGE('',*,*,#5328,.F.);
#6809=ORIENTED_EDGE('',*,*,#5330,.F.);
#6810=ORIENTED_EDGE('',*,*,#5331,.T.);
#6811=ORIENTED_EDGE('',*,*,#5332,.F.);
#6812=ORIENTED_EDGE('',*,*,#5331,.F.);
#6813=ORIENTED_EDGE('',*,*,#5333,.F.);
#6814=ORIENTED_EDGE('',*,*,#5334,.T.);
#6815=ORIENTED_EDGE('',*,*,#5335,.F.);
#6816=ORIENTED_EDGE('',*,*,#5334,.F.);
#6817=ORIENTED_EDGE('',*,*,#5336,.F.);
#6818=ORIENTED_EDGE('',*,*,#5337,.T.);
#6819=ORIENTED_EDGE('',*,*,#5338,.F.);
#6820=ORIENTED_EDGE('',*,*,#5337,.F.);
#6821=ORIENTED_EDGE('',*,*,#5339,.F.);
#6822=ORIENTED_EDGE('',*,*,#5340,.T.);
#6823=ORIENTED_EDGE('',*,*,#5341,.F.);
#6824=ORIENTED_EDGE('',*,*,#5340,.F.);
#6825=ORIENTED_EDGE('',*,*,#5342,.F.);
#6826=ORIENTED_EDGE('',*,*,#5343,.T.);
#6827=ORIENTED_EDGE('',*,*,#5344,.F.);
#6828=ORIENTED_EDGE('',*,*,#5343,.F.);
#6829=ORIENTED_EDGE('',*,*,#5345,.F.);
#6830=ORIENTED_EDGE('',*,*,#5346,.T.);
#6831=ORIENTED_EDGE('',*,*,#5347,.F.);
#6832=ORIENTED_EDGE('',*,*,#5346,.F.);
#6833=ORIENTED_EDGE('',*,*,#5348,.F.);
#6834=ORIENTED_EDGE('',*,*,#5349,.F.);
#6835=ORIENTED_EDGE('',*,*,#5350,.F.);
#6836=ORIENTED_EDGE('',*,*,#5351,.T.);
#6837=ORIENTED_EDGE('',*,*,#5344,.T.);
#6838=ORIENTED_EDGE('',*,*,#5352,.F.);
#6839=ORIENTED_EDGE('',*,*,#5353,.T.);
#6840=ORIENTED_EDGE('',*,*,#5354,.T.);
#6841=ORIENTED_EDGE('',*,*,#5355,.F.);
#6842=ORIENTED_EDGE('',*,*,#5341,.T.);
#6843=ORIENTED_EDGE('',*,*,#5356,.T.);
#6844=ORIENTED_EDGE('',*,*,#5350,.T.);
#6845=ORIENTED_EDGE('',*,*,#5357,.F.);
#6846=ORIENTED_EDGE('',*,*,#5358,.F.);
#6847=ORIENTED_EDGE('',*,*,#5359,.T.);
#6848=ORIENTED_EDGE('',*,*,#5360,.T.);
#6849=ORIENTED_EDGE('',*,*,#5361,.F.);
#6850=ORIENTED_EDGE('',*,*,#5354,.F.);
#6851=ORIENTED_EDGE('',*,*,#5352,.T.);
#6852=ORIENTED_EDGE('',*,*,#5362,.T.);
#6853=ORIENTED_EDGE('',*,*,#5363,.F.);
#6854=ORIENTED_EDGE('',*,*,#5364,.F.);
#6855=ORIENTED_EDGE('',*,*,#5365,.T.);
#6856=ORIENTED_EDGE('',*,*,#5366,.F.);
#6857=ORIENTED_EDGE('',*,*,#5362,.F.);
#6858=ORIENTED_EDGE('',*,*,#5355,.T.);
#6859=ORIENTED_EDGE('',*,*,#5361,.T.);
#6860=ORIENTED_EDGE('',*,*,#5367,.T.);
#6861=ORIENTED_EDGE('',*,*,#5357,.T.);
#6862=ORIENTED_EDGE('',*,*,#5349,.T.);
#6863=ORIENTED_EDGE('',*,*,#5347,.T.);
#6864=ORIENTED_EDGE('',*,*,#5338,.T.);
#6865=ORIENTED_EDGE('',*,*,#5335,.T.);
#6866=ORIENTED_EDGE('',*,*,#5332,.T.);
#6867=ORIENTED_EDGE('',*,*,#5329,.T.);
#6868=ORIENTED_EDGE('',*,*,#5348,.T.);
#6869=ORIENTED_EDGE('',*,*,#5368,.T.);
#6870=ORIENTED_EDGE('',*,*,#5369,.F.);
#6871=ORIENTED_EDGE('',*,*,#5365,.F.);
#6872=ORIENTED_EDGE('',*,*,#5364,.T.);
#6873=ORIENTED_EDGE('',*,*,#5370,.F.);
#6874=ORIENTED_EDGE('',*,*,#5368,.F.);
#6875=ORIENTED_EDGE('',*,*,#5351,.F.);
#6876=ORIENTED_EDGE('',*,*,#5356,.F.);
#6877=ORIENTED_EDGE('',*,*,#5371,.T.);
#6878=ORIENTED_EDGE('',*,*,#5359,.F.);
#6879=ORIENTED_EDGE('',*,*,#5353,.F.);
#6880=ORIENTED_EDGE('',*,*,#5345,.T.);
#6881=ORIENTED_EDGE('',*,*,#5336,.T.);
#6882=ORIENTED_EDGE('',*,*,#5333,.T.);
#6883=ORIENTED_EDGE('',*,*,#5330,.T.);
#6884=ORIENTED_EDGE('',*,*,#5327,.T.);
#6885=ORIENTED_EDGE('',*,*,#5370,.T.);
#6886=ORIENTED_EDGE('',*,*,#5363,.T.);
#6887=ORIENTED_EDGE('',*,*,#5366,.T.);
#6888=ORIENTED_EDGE('',*,*,#5369,.T.);
#6889=ORIENTED_EDGE('',*,*,#5371,.F.);
#6890=ORIENTED_EDGE('',*,*,#5358,.T.);
#6891=ORIENTED_EDGE('',*,*,#5367,.F.);
#6892=ORIENTED_EDGE('',*,*,#5360,.F.);
#6893=ORIENTED_EDGE('',*,*,#5339,.T.);
#6894=ORIENTED_EDGE('',*,*,#5342,.T.);
#8422=CYLINDRICAL_SURFACE('',#9863,0.165);
#8423=CYLINDRICAL_SURFACE('',#9866,0.165);
#8424=CYLINDRICAL_SURFACE('',#9869,0.165);
#8425=CYLINDRICAL_SURFACE('',#9872,0.165);
#8426=CYLINDRICAL_SURFACE('',#9875,0.225);
#8427=CYLINDRICAL_SURFACE('',#9878,0.225);
#8428=CYLINDRICAL_SURFACE('',#9881,1.6);
#8710=ADVANCED_FACE('',(#1412),#8422,.F.);
#8711=ADVANCED_FACE('',(#1413),#8423,.F.);
#8712=ADVANCED_FACE('',(#1414),#8424,.F.);
#8713=ADVANCED_FACE('',(#1415),#8425,.F.);
#8714=ADVANCED_FACE('',(#1416),#8426,.F.);
#8715=ADVANCED_FACE('',(#1417),#8427,.F.);
#8716=ADVANCED_FACE('',(#1418),#8428,.F.);
#8717=ADVANCED_FACE('',(#1419,#806),#1088,.T.);
#8718=ADVANCED_FACE('',(#1420,#807),#1089,.T.);
#8719=ADVANCED_FACE('',(#1421),#1090,.T.);
#8720=ADVANCED_FACE('',(#1422),#1091,.T.);
#8721=ADVANCED_FACE('',(#1423),#1092,.T.);
#8722=ADVANCED_FACE('',(#1424,#808,#809,#810,#811,#812),#1093,.T.);
#8723=ADVANCED_FACE('',(#1425),#1094,.T.);
#8724=ADVANCED_FACE('',(#1426,#813,#814,#815,#816,#817),#1095,.T.);
#8725=ADVANCED_FACE('',(#1427),#1096,.T.);
#8726=ADVANCED_FACE('',(#1428,#818,#819),#1097,.F.);
#9085=CLOSED_SHELL('',(#8710,#8711,#8712,#8713,#8714,#8715,#8716,#8717,
#8718,#8719,#8720,#8721,#8722,#8723,#8724,#8725,#8726));
#9862=AXIS2_PLACEMENT_3D('',#14479,#11523,#11524);
#9863=AXIS2_PLACEMENT_3D('',#14480,#11525,#11526);
#9864=AXIS2_PLACEMENT_3D('',#14482,#11527,#11528);
#9865=AXIS2_PLACEMENT_3D('',#14485,#11530,#11531);
#9866=AXIS2_PLACEMENT_3D('',#14486,#11532,#11533);
#9867=AXIS2_PLACEMENT_3D('',#14488,#11534,#11535);
#9868=AXIS2_PLACEMENT_3D('',#14491,#11537,#11538);
#9869=AXIS2_PLACEMENT_3D('',#14492,#11539,#11540);
#9870=AXIS2_PLACEMENT_3D('',#14494,#11541,#11542);
#9871=AXIS2_PLACEMENT_3D('',#14497,#11544,#11545);
#9872=AXIS2_PLACEMENT_3D('',#14498,#11546,#11547);
#9873=AXIS2_PLACEMENT_3D('',#14500,#11548,#11549);
#9874=AXIS2_PLACEMENT_3D('',#14503,#11551,#11552);
#9875=AXIS2_PLACEMENT_3D('',#14504,#11553,#11554);
#9876=AXIS2_PLACEMENT_3D('',#14506,#11555,#11556);
#9877=AXIS2_PLACEMENT_3D('',#14509,#11558,#11559);
#9878=AXIS2_PLACEMENT_3D('',#14510,#11560,#11561);
#9879=AXIS2_PLACEMENT_3D('',#14512,#11562,#11563);
#9880=AXIS2_PLACEMENT_3D('',#14515,#11565,#11566);
#9881=AXIS2_PLACEMENT_3D('',#14516,#11567,#11568);
#9882=AXIS2_PLACEMENT_3D('',#14518,#11569,#11570);
#9883=AXIS2_PLACEMENT_3D('',#14521,#11572,#11573);
#9884=AXIS2_PLACEMENT_3D('',#14522,#11574,#11575);
#9885=AXIS2_PLACEMENT_3D('',#14531,#11580,#11581);
#9886=AXIS2_PLACEMENT_3D('',#14540,#11586,#11587);
#9887=AXIS2_PLACEMENT_3D('',#14546,#11591,#11592);
#9888=AXIS2_PLACEMENT_3D('',#14552,#11596,#11597);
#9889=AXIS2_PLACEMENT_3D('',#14558,#11601,#11602);
#9890=AXIS2_PLACEMENT_3D('',#14563,#11606,#11607);
#9891=AXIS2_PLACEMENT_3D('',#14567,#11610,#11611);
#9892=AXIS2_PLACEMENT_3D('',#14570,#11614,#11615);
#9893=AXIS2_PLACEMENT_3D('',#14571,#11616,#11617);
#11523=DIRECTION('axis',(0.,0.,1.));
#11524=DIRECTION('refdir',(1.,0.,0.));
#11525=DIRECTION('center_axis',(1.,0.,0.));
#11526=DIRECTION('ref_axis',(0.,0.,-1.));
#11527=DIRECTION('center_axis',(1.,0.,0.));
#11528=DIRECTION('ref_axis',(0.,0.,-1.));
#11529=DIRECTION('',(1.,0.,0.));
#11530=DIRECTION('center_axis',(-1.,0.,0.));
#11531=DIRECTION('ref_axis',(0.,0.,-1.));
#11532=DIRECTION('center_axis',(1.,0.,0.));
#11533=DIRECTION('ref_axis',(0.,0.,-1.));
#11534=DIRECTION('center_axis',(1.,0.,0.));
#11535=DIRECTION('ref_axis',(0.,0.,-1.));
#11536=DIRECTION('',(1.,0.,0.));
#11537=DIRECTION('center_axis',(-1.,0.,0.));
#11538=DIRECTION('ref_axis',(0.,0.,-1.));
#11539=DIRECTION('center_axis',(1.,0.,0.));
#11540=DIRECTION('ref_axis',(0.,0.,-1.));
#11541=DIRECTION('center_axis',(1.,0.,0.));
#11542=DIRECTION('ref_axis',(0.,0.,-1.));
#11543=DIRECTION('',(1.,0.,0.));
#11544=DIRECTION('center_axis',(-1.,0.,0.));
#11545=DIRECTION('ref_axis',(0.,0.,-1.));
#11546=DIRECTION('center_axis',(1.,0.,0.));
#11547=DIRECTION('ref_axis',(0.,0.,-1.));
#11548=DIRECTION('center_axis',(1.,0.,0.));
#11549=DIRECTION('ref_axis',(0.,0.,-1.));
#11550=DIRECTION('',(1.,0.,0.));
#11551=DIRECTION('center_axis',(-1.,0.,0.));
#11552=DIRECTION('ref_axis',(0.,0.,-1.));
#11553=DIRECTION('center_axis',(0.,0.,1.));
#11554=DIRECTION('ref_axis',(1.,0.,0.));
#11555=DIRECTION('center_axis',(0.,0.,1.));
#11556=DIRECTION('ref_axis',(1.,0.,0.));
#11557=DIRECTION('',(0.,0.,1.));
#11558=DIRECTION('center_axis',(0.,0.,-1.));
#11559=DIRECTION('ref_axis',(1.,0.,0.));
#11560=DIRECTION('center_axis',(0.,0.,1.));
#11561=DIRECTION('ref_axis',(1.,0.,0.));
#11562=DIRECTION('center_axis',(0.,0.,1.));
#11563=DIRECTION('ref_axis',(1.,0.,0.));
#11564=DIRECTION('',(0.,0.,1.));
#11565=DIRECTION('center_axis',(0.,0.,-1.));
#11566=DIRECTION('ref_axis',(1.,0.,0.));
#11567=DIRECTION('center_axis',(1.,0.,0.));
#11568=DIRECTION('ref_axis',(0.,0.,-1.));
#11569=DIRECTION('center_axis',(1.,0.,0.));
#11570=DIRECTION('ref_axis',(0.,0.,-1.));
#11571=DIRECTION('',(1.,0.,0.));
#11572=DIRECTION('center_axis',(-1.,0.,0.));
#11573=DIRECTION('ref_axis',(0.,0.,-1.));
#11574=DIRECTION('center_axis',(0.,0.,1.));
#11575=DIRECTION('ref_axis',(0.,-1.,0.));
#11576=DIRECTION('',(-1.,0.,0.));
#11577=DIRECTION('',(0.,-1.,0.));
#11578=DIRECTION('',(1.,0.,0.));
#11579=DIRECTION('',(0.,-1.,0.));
#11580=DIRECTION('center_axis',(0.,0.,1.));
#11581=DIRECTION('ref_axis',(0.,-1.,0.));
#11582=DIRECTION('',(1.,0.,0.));
#11583=DIRECTION('',(0.,-1.,0.));
#11584=DIRECTION('',(1.,0.,0.));
#11585=DIRECTION('',(0.,-1.,0.));
#11586=DIRECTION('center_axis',(0.,1.,0.));
#11587=DIRECTION('ref_axis',(0.,0.,1.));
#11588=DIRECTION('',(0.,0.,1.));
#11589=DIRECTION('',(0.,0.,1.));
#11590=DIRECTION('',(1.,0.,0.));
#11591=DIRECTION('center_axis',(0.,-1.,0.));
#11592=DIRECTION('ref_axis',(0.,0.,-1.));
#11593=DIRECTION('',(0.,0.,-1.));
#11594=DIRECTION('',(1.,0.,0.));
#11595=DIRECTION('',(0.,0.,-1.));
#11596=DIRECTION('center_axis',(0.,-1.,0.));
#11597=DIRECTION('ref_axis',(1.,0.,0.));
#11598=DIRECTION('',(0.,0.,1.));
#11599=DIRECTION('',(1.,0.,0.));
#11600=DIRECTION('',(0.,0.,1.));
#11601=DIRECTION('center_axis',(1.,0.,0.));
#11602=DIRECTION('ref_axis',(0.,1.,0.));
#11603=DIRECTION('',(0.,0.,1.));
#11604=DIRECTION('',(0.,1.,0.));
#11605=DIRECTION('',(0.,1.,0.));
#11606=DIRECTION('center_axis',(0.,1.,0.));
#11607=DIRECTION('ref_axis',(-1.,0.,0.));
#11608=DIRECTION('',(0.,0.,1.));
#11609=DIRECTION('',(-1.,0.,0.));
#11610=DIRECTION('center_axis',(-1.,0.,0.));
#11611=DIRECTION('ref_axis',(0.,-1.,0.));
#11612=DIRECTION('',(0.,-1.,0.));
#11613=DIRECTION('',(0.,-1.,0.));
#11614=DIRECTION('center_axis',(0.,0.,1.));
#11615=DIRECTION('ref_axis',(1.,0.,0.));
#11616=DIRECTION('center_axis',(0.,0.,1.));
#11617=DIRECTION('ref_axis',(1.,0.,0.));
#14479=CARTESIAN_POINT('',(0.,0.,0.));
#14480=CARTESIAN_POINT('Origin',(10.6,-1.4142135623731,2.58578643762691));
#14481=CARTESIAN_POINT('',(10.7,-1.4142135623731,2.75078643762691));
#14482=CARTESIAN_POINT('Origin',(10.7,-1.4142135623731,2.58578643762691));
#14483=CARTESIAN_POINT('',(12.3,-1.4142135623731,2.75078643762691));
#14484=CARTESIAN_POINT('',(10.6,-1.4142135623731,2.75078643762691));
#14485=CARTESIAN_POINT('Origin',(12.3,-1.4142135623731,2.58578643762691));
#14486=CARTESIAN_POINT('Origin',(10.6,-1.41421356237309,5.41421356237309));
#14487=CARTESIAN_POINT('',(10.7,-1.41421356237309,5.57921356237309));
#14488=CARTESIAN_POINT('Origin',(10.7,-1.41421356237309,5.41421356237309));
#14489=CARTESIAN_POINT('',(12.3,-1.41421356237309,5.57921356237309));
#14490=CARTESIAN_POINT('',(10.6,-1.41421356237309,5.57921356237309));
#14491=CARTESIAN_POINT('Origin',(12.3,-1.41421356237309,5.41421356237309));
#14492=CARTESIAN_POINT('Origin',(10.6,1.4142135623731,5.41421356237309));
#14493=CARTESIAN_POINT('',(10.7,1.4142135623731,5.57921356237309));
#14494=CARTESIAN_POINT('Origin',(10.7,1.4142135623731,5.41421356237309));
#14495=CARTESIAN_POINT('',(12.3,1.4142135623731,5.57921356237309));
#14496=CARTESIAN_POINT('',(10.6,1.4142135623731,5.57921356237309));
#14497=CARTESIAN_POINT('Origin',(12.3,1.4142135623731,5.41421356237309));
#14498=CARTESIAN_POINT('Origin',(10.6,1.41421356237309,2.5857864376269));
#14499=CARTESIAN_POINT('',(10.7,1.41421356237309,2.7507864376269));
#14500=CARTESIAN_POINT('Origin',(10.7,1.41421356237309,2.5857864376269));
#14501=CARTESIAN_POINT('',(12.3,1.41421356237309,2.7507864376269));
#14502=CARTESIAN_POINT('',(10.6,1.41421356237309,2.7507864376269));
#14503=CARTESIAN_POINT('Origin',(12.3,1.41421356237309,2.5857864376269));
#14504=CARTESIAN_POINT('Origin',(11.5,-3.,0.9));
#14505=CARTESIAN_POINT('',(11.275,-3.,1.));
#14506=CARTESIAN_POINT('Origin',(11.5,-3.,1.));
#14507=CARTESIAN_POINT('',(11.275,-3.,1.8));
#14508=CARTESIAN_POINT('',(11.275,-3.,0.9));
#14509=CARTESIAN_POINT('Origin',(11.5,-3.,1.8));
#14510=CARTESIAN_POINT('Origin',(11.5,3.,0.9));
#14511=CARTESIAN_POINT('',(11.275,3.,1.));
#14512=CARTESIAN_POINT('Origin',(11.5,3.,1.));
#14513=CARTESIAN_POINT('',(11.275,3.,1.8));
#14514=CARTESIAN_POINT('',(11.275,3.,0.9));
#14515=CARTESIAN_POINT('Origin',(11.5,3.,1.8));
#14516=CARTESIAN_POINT('Origin',(10.6,0.,4.));
#14517=CARTESIAN_POINT('',(10.7,-1.95943487863577E-16,5.6));
#14518=CARTESIAN_POINT('Origin',(10.7,0.,4.));
#14519=CARTESIAN_POINT('',(12.3,1.95943487863577E-16,5.6));
#14520=CARTESIAN_POINT('',(10.6,-1.95943487863577E-16,5.6));
#14521=CARTESIAN_POINT('Origin',(12.3,0.,4.));
#14522=CARTESIAN_POINT('Origin',(10.7,3.6,1.8));
#14523=CARTESIAN_POINT('',(12.3,2.4,1.8));
#14524=CARTESIAN_POINT('',(10.7,2.4,1.8));
#14525=CARTESIAN_POINT('',(11.5,2.4,1.8));
#14526=CARTESIAN_POINT('',(12.3,3.6,1.8));
#14527=CARTESIAN_POINT('',(12.3,3.6,1.8));
#14528=CARTESIAN_POINT('',(10.7,3.6,1.8));
#14529=CARTESIAN_POINT('',(10.7,3.6,1.8));
#14530=CARTESIAN_POINT('',(10.7,3.6,1.8));
#14531=CARTESIAN_POINT('Origin',(10.7,3.6,1.8));
#14532=CARTESIAN_POINT('',(10.7,-2.4,1.8));
#14533=CARTESIAN_POINT('',(12.3,-2.4,1.8));
#14534=CARTESIAN_POINT('',(10.7,-2.4,1.8));
#14535=CARTESIAN_POINT('',(10.7,-3.6,1.8));
#14536=CARTESIAN_POINT('',(10.7,3.6,1.8));
#14537=CARTESIAN_POINT('',(12.3,-3.6,1.8));
#14538=CARTESIAN_POINT('',(10.7,-3.6,1.8));
#14539=CARTESIAN_POINT('',(12.3,3.6,1.8));
#14540=CARTESIAN_POINT('Origin',(10.7,3.6,1.));
#14541=CARTESIAN_POINT('',(10.7,3.6,1.));
#14542=CARTESIAN_POINT('',(10.7,3.6,1.));
#14543=CARTESIAN_POINT('',(12.3,3.6,1.));
#14544=CARTESIAN_POINT('',(12.3,3.6,1.));
#14545=CARTESIAN_POINT('',(10.7,3.6,1.));
#14546=CARTESIAN_POINT('Origin',(10.7,-3.6,1.8));
#14547=CARTESIAN_POINT('',(10.7,-3.6,1.));
#14548=CARTESIAN_POINT('',(10.7,-3.6,1.8));
#14549=CARTESIAN_POINT('',(12.3,-3.6,1.));
#14550=CARTESIAN_POINT('',(10.7,-3.6,1.));
#14551=CARTESIAN_POINT('',(12.3,-3.6,1.8));
#14552=CARTESIAN_POINT('Origin',(10.7,-2.4,1.));
#14553=CARTESIAN_POINT('',(12.3,-2.4,6.5));
#14554=CARTESIAN_POINT('',(12.3,-2.4,1.));
#14555=CARTESIAN_POINT('',(10.7,-2.4,6.5));
#14556=CARTESIAN_POINT('',(10.7,-2.4,6.5));
#14557=CARTESIAN_POINT('',(10.7,-2.4,1.));
#14558=CARTESIAN_POINT('Origin',(12.3,-2.4,1.));
#14559=CARTESIAN_POINT('',(12.3,2.4,6.5));
#14560=CARTESIAN_POINT('',(12.3,2.4,1.));
#14561=CARTESIAN_POINT('',(12.3,-2.4,6.5));
#14562=CARTESIAN_POINT('',(12.3,-3.6,1.));
#14563=CARTESIAN_POINT('Origin',(12.3,2.4,1.));
#14564=CARTESIAN_POINT('',(10.7,2.4,6.5));
#14565=CARTESIAN_POINT('',(10.7,2.4,1.));
#14566=CARTESIAN_POINT('',(12.3,2.4,6.5));
#14567=CARTESIAN_POINT('Origin',(10.7,2.4,1.));
#14568=CARTESIAN_POINT('',(10.7,2.4,6.5));
#14569=CARTESIAN_POINT('',(10.7,2.4,1.));
#14570=CARTESIAN_POINT('Origin',(11.5,0.,6.5));
#14571=CARTESIAN_POINT('Origin',(11.5,0.,1.));
#16714=UNCERTAINTY_MEASURE_WITH_UNIT(LENGTH_MEASURE(0.001),#16800,
'DISTANCE_ACCURACY_VALUE',
'Maximum model space distance between geometric entities at asserted c
onnectivities');
#16750=UNCERTAINTY_MEASURE_WITH_UNIT(LENGTH_MEASURE(0.001),#16800,
'DISTANCE_ACCURACY_VALUE',
'Maximum model space distance between geometric entities at asserted c
onnectivities');
#16763=(
GEOMETRIC_REPRESENTATION_CONTEXT(3)
GLOBAL_UNCERTAINTY_ASSIGNED_CONTEXT((#16714))
GLOBAL_UNIT_ASSIGNED_CONTEXT((#16800,#16802,#16803))
REPRESENTATION_CONTEXT('','3D')
);
#16799=(
GEOMETRIC_REPRESENTATION_CONTEXT(3)
GLOBAL_UNCERTAINTY_ASSIGNED_CONTEXT((#16750))
GLOBAL_UNIT_ASSIGNED_CONTEXT((#16800,#16802,#16803))
REPRESENTATION_CONTEXT('','3D')
);
#16800=(
LENGTH_UNIT()
NAMED_UNIT(*)
SI_UNIT(.CENTI.,.METRE.)
);
#16802=(
NAMED_UNIT(*)
PLANE_ANGLE_UNIT()
SI_UNIT($,.RADIAN.)
);
#16803=(
NAMED_UNIT(*)
SI_UNIT($,.STERADIAN.)
SOLID_ANGLE_UNIT()
);
#16816=SHAPE_DEFINITION_REPRESENTATION(#16864,#17025);
#16864=PRODUCT_DEFINITION_SHAPE('',$,#17074);
#17025=SHAPE_REPRESENTATION('',(#9862),#16763);
#17061=PRODUCT_DEFINITION_CONTEXT('part definition',#17207,'design');
#17074=PRODUCT_DEFINITION('Screw bearing post (1)',
'Screw bearing post (1)',#17122,#17061);
#17122=PRODUCT_DEFINITION_FORMATION('',$,#17221);
#17207=APPLICATION_CONTEXT(
'Core Data for Automotive Mechanical Design Process');
#17208=PRODUCT_CONTEXT('part definition',#17207,'mechanical');
#17221=PRODUCT('Screw bearing post (1)','Screw bearing post (1)',
'Screw bearing post (1)',(#17208));
#17327=COLOUR_RGB('Black',0.12,0.14,0.17);
#17328=FILL_AREA_STYLE_COLOUR('',#17327);
#17329=FILL_AREA_STYLE('',(#17328));
#17330=SURFACE_STYLE_FILL_AREA(#17329);
#17331=SURFACE_SIDE_STYLE('',(#17330));
#17332=SURFACE_STYLE_USAGE(.BOTH.,#17331);
#17333=PRESENTATION_STYLE_ASSIGNMENT((#17332));
ENDSEC;
END-ISO-10303-21;
